ISO-10303-21;
HEADER;
FILE_DESCRIPTION (('STEP AP214'),
    '1' );
FILE_NAME ('din_6885_2_a_6_x_6_x_25.step',
    '2026-11-01T06:29:40',
    ( '' ),
    ( '' ),
    'SwSTEP 2.0',
    'SolidWorks 2024',
    '' );
FILE_SCHEMA (( 'AUTOMOTIVE_DESIGN' ));
ENDSEC;

DATA;
#22=DIRECTION ( 'NONE',  ( 6.123031769111888756E-17, -1.000000000000000000, -3.749151804555344967E-33 ) ) ;
#141=AXIS2_PLACEMENT_3D ( 'NONE', #16061, #16163, #8419 ) ;
#195=CARTESIAN_POINT ( 'NONE',  ( -3.000000000000000000, -1.836909530733565148E-16, 22.00000000000000000 ) ) ;
#210=DIRECTION ( 'NONE',  ( 6.123031769111888756E-17, 0.000000000000000000, 1.000000000000000000 ) ) ;
#264=DIRECTION ( 'NONE',  ( 6.123031769111888756E-17, -1.000000000000000000, -3.749151804555344967E-33 ) ) ;
#365=EDGE_LOOP ( 'NONE', ( #5974, #11325, #14847, #11434 ) ) ;
#559=FILL_AREA_STYLE_COLOUR ( '', #17283 ) ;
#727=CARTESIAN_POINT ( 'NONE',  ( 3.000000000000000000, 6.000000000000000000, 3.000000000000000000 ) ) ;
#745=( NAMED_UNIT ( * ) SI_UNIT ( $, .STERADIAN. ) SOLID_ANGLE_UNIT ( ) );
#849=ORIENTED_EDGE ( 'NONE', *, *, #19801, .F. ) ;
#954=EDGE_CURVE ( 'NONE', #3178, #10041, #19828, .T. ) ;
#1028=UNCERTAINTY_MEASURE_WITH_UNIT (LENGTH_MEASURE( 1.000000000000000082E-05 ), #3866, 'distance_accuracy_value', 'NONE');
#1077=ORIENTED_EDGE ( 'NONE', *, *, #16118, .T. ) ;
#1158=CARTESIAN_POINT ( 'NONE',  ( -3.000000000000000000, -1.836909530733565148E-16, 22.00000000000000000 ) ) ;
#1264=MANIFOLD_SOLID_BREP ( 'Imported1', #20162 ) ;
#1377=AXIS2_PLACEMENT_3D ( 'NONE', #19114, #264, #12857 ) ;
#1388=AXIS2_PLACEMENT_3D ( 'NONE', #17608, #9779, #17190 ) ;
#1497=PRODUCT ( 'din_6885_2_a_6_x_6_x_25', 'din_6885_2_a_6_x_6_x_25', '', ( #10559 ) ) ;
#1607=DIRECTION ( 'NONE',  ( -6.123031769111888756E-17, 1.000000000000000000, 3.749151804555344967E-33 ) ) ;
#1689=LINE ( 'NONE', #2941, #9628 ) ;
#1826=EDGE_CURVE ( 'NONE', #19851, #13429, #11455, .T. ) ;
#1868=DIRECTION ( 'NONE',  ( 6.123031769111888756E-17, 0.000000000000000000, 1.000000000000000000 ) ) ;
#1922=SHAPE_REPRESENTATION ( 'din_6885_2_a_6_x_6_x_25', ( #2741 ), #7323 ) ;
#1978=ORIENTED_EDGE ( 'NONE', *, *, #12942, .F. ) ;
#2033=CARTESIAN_POINT ( 'NONE',  ( 1.836909530733565148E-16, 0.000000000000000000, 3.000000000000000000 ) ) ;
#2125=AXIS2_PLACEMENT_3D ( 'NONE', #17346, #18978, #1868 ) ;
#2166=EDGE_CURVE ( 'NONE', #19208, #4579, #2902, .T. ) ;
#2323=FACE_OUTER_BOUND ( 'NONE', #10236, .T. ) ;
#2467=CARTESIAN_POINT ( 'NONE',  ( 3.000000000000000000, 1.836909530733565148E-16, 12.50000000000000000 ) ) ;
#2676=ORIENTED_EDGE ( 'NONE', *, *, #1826, .F. ) ;
#2704=CARTESIAN_POINT ( 'NONE',  ( 1.530757942277970587E-15, 0.000000000000000000, 24.99999999999999645 ) ) ;
#2741=AXIS2_PLACEMENT_3D ( 'NONE', #5042, #3500, #8234 ) ;
#2884=EDGE_CURVE ( 'NONE', #17060, #13429, #12146, .T. ) ;
#2902=LINE ( 'NONE', #2704, #7758 ) ;
#2909=ORIENTED_EDGE ( 'NONE', *, *, #12156, .F. ) ;
#2941=CARTESIAN_POINT ( 'NONE',  ( 3.000000000000000000, 1.836909530733570325E-16, 3.000000000000000000 ) ) ;
#3175=VECTOR ( 'NONE', #13887, 1000.000000000000000 ) ;
#3178=VERTEX_POINT ( 'NONE', #3688 ) ;
#3335=PRODUCT_DEFINITION_SHAPE ( 'NONE', 'NONE',  #19657 ) ;
#3500=DIRECTION ( 'NONE',  ( 0.000000000000000000, 0.000000000000000000, 1.000000000000000000 ) ) ;
#3545=FACE_OUTER_BOUND ( 'NONE', #19371, .T. ) ;
#3668=DIRECTION ( 'NONE',  ( 6.123031769111888756E-17, 0.000000000000000000, 1.000000000000000000 ) ) ;
#3688=CARTESIAN_POINT ( 'NONE',  ( -3.000000000000000000, -1.836909530733565148E-16, 3.000000000000000000 ) ) ;
#3721=DIRECTION ( 'NONE',  ( 6.123031769111888756E-17, 0.000000000000000000, 1.000000000000000000 ) ) ;
#3846=ADVANCED_FACE ( 'NONE', ( #13597 ), #16315, .T. ) ;
#3866=( LENGTH_UNIT ( ) NAMED_UNIT ( * ) SI_UNIT ( .MILLI., .METRE. ) );
#4002=ORIENTED_EDGE ( 'NONE', *, *, #12942, .T. ) ;
#4395=( LENGTH_UNIT ( ) NAMED_UNIT ( * ) SI_UNIT ( .MILLI., .METRE. ) );
#4509=FACE_OUTER_BOUND ( 'NONE', #8511, .T. ) ;
#4568=AXIS2_PLACEMENT_3D ( 'NONE', #13347, #14457, #19483 ) ;
#4579=VERTEX_POINT ( 'NONE', #5129 ) ;
#4681=ADVANCED_BREP_SHAPE_REPRESENTATION ( '', ( #1264, #2741 ), #7323 ) ;
#4772=ADVANCED_FACE ( 'NONE', ( #8714 ), #7074, .T. ) ;
#5027=ADVANCED_FACE ( 'NONE', ( #3545 ), #13140, .F. ) ;
#5042=CARTESIAN_POINT ( 'NONE',  ( 0.000000000000000000, 0.000000000000000000, 0.000000000000000000 ) ) ;
#5105=VERTEX_POINT ( 'NONE', #10035 ) ;
#5129=CARTESIAN_POINT ( 'NONE',  ( 1.347066989204613998E-15, -1.203706215242022682E-32, 24.99999999999999645 ) ) ;
#5175=DIRECTION ( 'NONE',  ( -6.123031769111888756E-17, 1.000000000000000000, 3.749151804555344967E-33 ) ) ;
#5228=ORIENTED_EDGE ( 'NONE', *, *, #1826, .T. ) ;
#5292=DIRECTION ( 'NONE',  ( 6.123031769111888756E-17, 0.000000000000000000, 1.000000000000000000 ) ) ;
#5314=PRESENTATION_STYLE_ASSIGNMENT (( #19313 ) ) ;
#5394=CARTESIAN_POINT ( 'NONE',  ( -1.836909530733565148E-16, 6.000000000000000000, 3.000000000000000000 ) ) ;
#5408=AXIS2_PLACEMENT_3D ( 'NONE', #12840, #19098, #14070 ) ;
#5585=CARTESIAN_POINT ( 'NONE',  ( 3.000000000000000000, 1.836909530733570325E-16, 3.000000000000000000 ) ) ;
#5670=ORIENTED_EDGE ( 'NONE', *, *, #19801, .T. ) ;
#5777=CARTESIAN_POINT ( 'NONE',  ( 3.000000000000000000, 1.836909530733565148E-16, 22.00000000000000000 ) ) ;
#5974=ORIENTED_EDGE ( 'NONE', *, *, #10255, .T. ) ;
#6038=CARTESIAN_POINT ( 'NONE',  ( -3.000000000000000000, 6.000000000000000000, 22.00000000000000000 ) ) ;
#6054=DIRECTION ( 'NONE',  ( -6.123031769111888756E-17, 1.000000000000000000, 3.749151804555344967E-33 ) ) ;
#6420=CIRCLE ( 'NONE', #141, 2.999999999999999112 ) ;
#6616=PLANE ( 'NONE',  #10687 ) ;
#6745=CIRCLE ( 'NONE', #5408, 2.999999999999999112 ) ;
#6830=CARTESIAN_POINT ( 'NONE',  ( -3.000000000000000000, -1.836909530733565148E-16, 12.50000000000000000 ) ) ;
#6861=ADVANCED_FACE ( 'NONE', ( #2323 ), #18191, .T. ) ;
#7074=CYLINDRICAL_SURFACE ( 'NONE', #18694, 2.999999999999999112 ) ;
#7180=DIRECTION ( 'NONE',  ( 6.123031769111888756E-17, -1.000000000000000000, -3.749151804555344967E-33 ) ) ;
#7323=( GEOMETRIC_REPRESENTATION_CONTEXT ( 3 ) GLOBAL_UNCERTAINTY_ASSIGNED_CONTEXT ( ( #13403 ) ) GLOBAL_UNIT_ASSIGNED_CONTEXT ( ( #4395, #13684, #15224 ) ) REPRESENTATION_CONTEXT ( 'NONE', 'WORKASPACE' ) );
#7389=CARTESIAN_POINT ( 'NONE',  ( -3.000000000000000000, -1.836909530733565148E-16, 3.000000000000000000 ) ) ;
#7393=LINE ( 'NONE', #17158, #19384 ) ;
#7586=DIRECTION ( 'NONE',  ( -6.123031769111888756E-17, 0.000000000000000000, -1.000000000000000000 ) ) ;
#7736=ORIENTED_EDGE ( 'NONE', *, *, #11599, .F. ) ;
#7758=VECTOR ( 'NONE', #22, 1000.000000000000000 ) ;
#7946=EDGE_LOOP ( 'NONE', ( #14213, #2909, #12824, #1077 ) ) ;
#8234=DIRECTION ( 'NONE',  ( 1.000000000000000000, 0.000000000000000000, 0.000000000000000000 ) ) ;
#8304=FILL_AREA_STYLE ('',( #559 ) ) ;
#8378=CIRCLE ( 'NONE', #12646, 2.999999999999999112 ) ;
#8419=DIRECTION ( 'NONE',  ( 6.123031769111888756E-17, 0.000000000000000000, 1.000000000000000000 ) ) ;
#8496=SURFACE_STYLE_FILL_AREA ( #8304 ) ;
#8511=EDGE_LOOP ( 'NONE', ( #5670, #8593, #11747, #10820 ) ) ;
#8524=CARTESIAN_POINT ( 'NONE',  ( 3.000000000000000000, 6.000000000000000000, 22.00000000000000000 ) ) ;
#8536=ORIENTED_EDGE ( 'NONE', *, *, #13554, .T. ) ;
#8593=ORIENTED_EDGE ( 'NONE', *, *, #13554, .F. ) ;
#8616=CARTESIAN_POINT ( 'NONE',  ( 1.347066989204613998E-15, 0.000000000000000000, 22.00000000000000000 ) ) ;
#8685=VECTOR ( 'NONE', #18822, 1000.000000000000000 ) ;
#8698=CARTESIAN_POINT ( 'NONE',  ( 9.796850830579020038E-16, 6.000000000000000000, 22.00000000000000000 ) ) ;
#8714=FACE_OUTER_BOUND ( 'NONE', #365, .T. ) ;
#8776=EDGE_LOOP ( 'NONE', ( #5228, #16040, #10743, #8536 ) ) ;
#9159=LINE ( 'NONE', #10809, #8685 ) ;
#9628=VECTOR ( 'NONE', #6054, 1000.000000000000000 ) ;
#9779=DIRECTION ( 'NONE',  ( -6.123031769111888756E-17, 1.000000000000000000, 3.749151804555346336E-33 ) ) ;
#9968=VERTEX_POINT ( 'NONE', #6038 ) ;
#10035=CARTESIAN_POINT ( 'NONE',  ( -3.000000000000000000, 6.000000000000000000, 3.000000000000000000 ) ) ;
#10041=VERTEX_POINT ( 'NONE', #1158 ) ;
#10178=EDGE_CURVE ( 'NONE', #4579, #17060, #6745, .T. ) ;
#10236=EDGE_LOOP ( 'NONE', ( #10244, #4002, #19418, #11416 ) ) ;
#10244=ORIENTED_EDGE ( 'NONE', *, *, #2166, .F. ) ;
#10255=EDGE_CURVE ( 'NONE', #13429, #19208, #8378, .T. ) ;
#10284=PRODUCT_DEFINITION_CONTEXT ( 'detailed design', #18282, 'design' ) ;
#10298=DIRECTION ( 'NONE',  ( 7.900838015626929923E-17, 8.586860021784410058E-33, -1.000000000000000000 ) ) ;
#10559=PRODUCT_CONTEXT ( 'NONE', #11576, 'mechanical' ) ;
#10610=PRODUCT_DEFINITION_FORMATION_WITH_SPECIFIED_SOURCE ( 'ANY', '', #1497, .NOT_KNOWN. ) ;
#10671=DIRECTION ( 'NONE',  ( 6.123031769111888756E-17, 0.000000000000000000, 1.000000000000000000 ) ) ;
#10687=AXIS2_PLACEMENT_3D ( 'NONE', #6830, #13120, #3721 ) ;
#10693=VECTOR ( 'NONE', #10671, 1000.000000000000000 ) ;
#10743=ORIENTED_EDGE ( 'NONE', *, *, #11599, .T. ) ;
#10809=CARTESIAN_POINT ( 'NONE',  ( -3.000000000000000000, -1.836909530733565148E-16, 3.000000000000000000 ) ) ;
#10820=ORIENTED_EDGE ( 'NONE', *, *, #12156, .T. ) ;
#10869=EDGE_CURVE ( 'NONE', #9968, #5105, #7393, .T. ) ;
#10976=AXIS2_PLACEMENT_3D ( 'NONE', #2033, #5175, #210 ) ;
#11028=CIRCLE ( 'NONE', #2125, 2.999999999999999112 ) ;
#11325=ORIENTED_EDGE ( 'NONE', *, *, #2166, .T. ) ;
#11416=ORIENTED_EDGE ( 'NONE', *, *, #12538, .T. ) ;
#11434=ORIENTED_EDGE ( 'NONE', *, *, #2884, .T. ) ;
#11455=LINE ( 'NONE', #19369, #15320 ) ;
#11530=AXIS2_PLACEMENT_3D ( 'NONE', #8616, #14914, #16870 ) ;
#11576=APPLICATION_CONTEXT ( 'automotive_design' ) ;
#11599=EDGE_CURVE ( 'NONE', #17060, #13107, #18756, .T. ) ;
#11700=EDGE_LOOP ( 'NONE', ( #849, #16673, #1978, #13238, #2676 ) ) ;
#11747=ORIENTED_EDGE ( 'NONE', *, *, #14133, .T. ) ;
#12146=LINE ( 'NONE', #5777, #3175 ) ;
#12156=EDGE_CURVE ( 'NONE', #3178, #5105, #9159, .T. ) ;
#12420=SHAPE_DEFINITION_REPRESENTATION ( #3335, #1922 ) ;
#12538=EDGE_CURVE ( 'NONE', #10041, #4579, #6420, .T. ) ;
#12646=AXIS2_PLACEMENT_3D ( 'NONE', #8698, #13360, #14687 ) ;
#12821=DIRECTION ( 'NONE',  ( 6.123031769111888756E-17, -1.000000000000000000, -3.749151804555344967E-33 ) ) ;
#12824=ORIENTED_EDGE ( 'NONE', *, *, #954, .T. ) ;
#12840=CARTESIAN_POINT ( 'NONE',  ( 1.347066989204613998E-15, 0.000000000000000000, 22.00000000000000000 ) ) ;
#12857=DIRECTION ( 'NONE',  ( 6.123031769111888756E-17, 0.000000000000000000, 1.000000000000000000 ) ) ;
#12865=AXIS2_PLACEMENT_3D ( 'NONE', #5394, #12821, #5292 ) ;
#12942=EDGE_CURVE ( 'NONE', #19208, #9968, #11028, .T. ) ;
#12970=CIRCLE ( 'NONE', #10976, 3.000000000000000000 ) ;
#13107=VERTEX_POINT ( 'NONE', #5585 ) ;
#13120=DIRECTION ( 'NONE',  ( -1.000000000000000000, -6.123031769111888756E-17, 6.123031769111888756E-17 ) ) ;
#13140=PLANE ( 'NONE',  #4568 ) ;
#13238=ORIENTED_EDGE ( 'NONE', *, *, #10255, .F. ) ;
#13347=CARTESIAN_POINT ( 'NONE',  ( 1.209468180989048008E-15, 2.719172340231729715E-32, 12.50000000000000000 ) ) ;
#13360=DIRECTION ( 'NONE',  ( 6.123031769111888756E-17, -1.000000000000000000, -3.749151804555344967E-33 ) ) ;
#13403=UNCERTAINTY_MEASURE_WITH_UNIT (LENGTH_MEASURE( 1.000000000000000082E-05 ), #4395, 'distance_accuracy_value', 'NONE');
#13429=VERTEX_POINT ( 'NONE', #8524 ) ;
#13531=CARTESIAN_POINT ( 'NONE',  ( 1.347066989204613998E-15, 6.000000000000000000, 24.99999999999999645 ) ) ;
#13554=EDGE_CURVE ( 'NONE', #13107, #19851, #1689, .T. ) ;
#13576=SHAPE_REPRESENTATION_RELATIONSHIP ( 'NONE' , 'NONE' ,  #1922, #4681 ) ;
#13597=FACE_OUTER_BOUND ( 'NONE', #8776, .T. ) ;
#13617=( GEOMETRIC_REPRESENTATION_CONTEXT ( 3 ) GLOBAL_UNCERTAINTY_ASSIGNED_CONTEXT ( ( #1028 ) ) GLOBAL_UNIT_ASSIGNED_CONTEXT ( ( #3866, #14879, #745 ) ) REPRESENTATION_CONTEXT ( 'NONE', 'WORKASPACE' ) );
#13684=( NAMED_UNIT ( * ) PLANE_ANGLE_UNIT ( ) SI_UNIT ( $, .RADIAN. ) );
#13688=ADVANCED_FACE ( 'NONE', ( #4509 ), #20261, .T. ) ;
#13734=AXIS2_PLACEMENT_3D ( 'NONE', #2467, #16410, #10298 ) ;
#13887=DIRECTION ( 'NONE',  ( -6.123031769111888756E-17, 1.000000000000000000, 3.749151804555344967E-33 ) ) ;
#14070=DIRECTION ( 'NONE',  ( 6.123031769111888756E-17, 0.000000000000000000, 1.000000000000000000 ) ) ;
#14133=EDGE_CURVE ( 'NONE', #13107, #3178, #12970, .T. ) ;
#14202=FACE_OUTER_BOUND ( 'NONE', #11700, .T. ) ;
#14213=ORIENTED_EDGE ( 'NONE', *, *, #10869, .T. ) ;
#14457=DIRECTION ( 'NONE',  ( -6.123031769111888756E-17, 1.000000000000000000, 3.749151804555346336E-33 ) ) ;
#14472=ORIENTED_EDGE ( 'NONE', *, *, #10178, .F. ) ;
#14496=ORIENTED_EDGE ( 'NONE', *, *, #954, .F. ) ;
#14602=STYLED_ITEM ( 'NONE', ( #5314 ), #1264 ) ;
#14687=DIRECTION ( 'NONE',  ( 6.123031769111888756E-17, 0.000000000000000000, 1.000000000000000000 ) ) ;
#14847=ORIENTED_EDGE ( 'NONE', *, *, #10178, .T. ) ;
#14879=( NAMED_UNIT ( * ) PLANE_ANGLE_UNIT ( ) SI_UNIT ( $, .RADIAN. ) );
#14914=DIRECTION ( 'NONE',  ( 6.123031769111888756E-17, -1.000000000000000000, -3.749151804555344967E-33 ) ) ;
#15005=CARTESIAN_POINT ( 'NONE',  ( 1.347066989204613998E-15, 0.000000000000000000, 22.00000000000000000 ) ) ;
#15083=ADVANCED_FACE ( 'NONE', ( #16211 ), #6616, .T. ) ;
#15131=VECTOR ( 'NONE', #1607, 1000.000000000000000 ) ;
#15224=( NAMED_UNIT ( * ) SI_UNIT ( $, .STERADIAN. ) SOLID_ANGLE_UNIT ( ) );
#15230=VECTOR ( 'NONE', #17414, 1000.000000000000000 ) ;
#15320=VECTOR ( 'NONE', #19060, 1000.000000000000000 ) ;
#15999=LINE ( 'NONE', #195, #15131 ) ;
#16040=ORIENTED_EDGE ( 'NONE', *, *, #2884, .F. ) ;
#16061=CARTESIAN_POINT ( 'NONE',  ( 1.347066989204613998E-15, 0.000000000000000000, 22.00000000000000000 ) ) ;
#16118=EDGE_CURVE ( 'NONE', #10041, #9968, #15999, .T. ) ;
#16163=DIRECTION ( 'NONE',  ( -6.123031769111888756E-17, 1.000000000000000000, 3.749151804555344967E-33 ) ) ;
#16211=FACE_OUTER_BOUND ( 'NONE', #7946, .T. ) ;
#16226=ORIENTED_EDGE ( 'NONE', *, *, #14133, .F. ) ;
#16315=PLANE ( 'NONE',  #13734 ) ;
#16410=DIRECTION ( 'NONE',  ( 1.000000000000000000, 6.123031769111888756E-17, 7.900838015626929923E-17 ) ) ;
#16673=ORIENTED_EDGE ( 'NONE', *, *, #10869, .F. ) ;
#16870=DIRECTION ( 'NONE',  ( 6.123031769111888756E-17, 0.000000000000000000, 1.000000000000000000 ) ) ;
#17060=VERTEX_POINT ( 'NONE', #17437 ) ;
#17119=CIRCLE ( 'NONE', #12865, 3.000000000000000000 ) ;
#17158=CARTESIAN_POINT ( 'NONE',  ( -3.000000000000000000, 6.000000000000000000, 3.000000000000000000 ) ) ;
#17190=DIRECTION ( 'NONE',  ( 6.123031769111888756E-17, 0.000000000000000000, 1.000000000000000000 ) ) ;
#17283=COLOUR_RGB ( '', 0.66274510, 0.83137255, 0.94901961) ;
#17346=CARTESIAN_POINT ( 'NONE',  ( 9.796850830579020038E-16, 6.000000000000000000, 22.00000000000000000 ) ) ;
#17414=DIRECTION ( 'NONE',  ( 7.900838015626929923E-17, 8.586860021784410058E-33, -1.000000000000000000 ) ) ;
#17437=CARTESIAN_POINT ( 'NONE',  ( 3.000000000000000000, 1.836909530733565148E-16, 22.00000000000000000 ) ) ;
#17608=CARTESIAN_POINT ( 'NONE',  ( 8.420862748423350279E-16, 6.000000000000000000, 12.50000000000000000 ) ) ;
#17974=SURFACE_SIDE_STYLE ('',( #8496 ) ) ;
#18191=CYLINDRICAL_SURFACE ( 'NONE', #11530, 2.999999999999999112 ) ;
#18282=APPLICATION_CONTEXT ( 'automotive_design' ) ;
#18694=AXIS2_PLACEMENT_3D ( 'NONE', #15005, #7180, #3668 ) ;
#18756=LINE ( 'NONE', #18851, #15230 ) ;
#18822=DIRECTION ( 'NONE',  ( -6.123031769111888756E-17, 1.000000000000000000, 3.749151804555344967E-33 ) ) ;
#18851=CARTESIAN_POINT ( 'NONE',  ( 3.000000000000000000, 1.836909530733565148E-16, 22.00000000000000000 ) ) ;
#18861=MECHANICAL_DESIGN_GEOMETRIC_PRESENTATION_REPRESENTATION('',(#14602),#13617);
#18978=DIRECTION ( 'NONE',  ( 6.123031769111888756E-17, -1.000000000000000000, -3.749151804555344967E-33 ) ) ;
#19022=PLANE ( 'NONE',  #1388 ) ;
#19060=DIRECTION ( 'NONE',  ( -7.900838015626929923E-17, -8.586860021784410058E-33, 1.000000000000000000 ) ) ;
#19098=DIRECTION ( 'NONE',  ( -6.123031769111888756E-17, 1.000000000000000000, 3.749151804555344967E-33 ) ) ;
#19114=CARTESIAN_POINT ( 'NONE',  ( 1.836909530733565148E-16, 0.000000000000000000, 3.000000000000000000 ) ) ;
#19208=VERTEX_POINT ( 'NONE', #13531 ) ;
#19313=SURFACE_STYLE_USAGE ( .BOTH. , #17974 ) ;
#19369=CARTESIAN_POINT ( 'NONE',  ( 3.000000000000000000, 6.000000000000000000, 22.00000000000000000 ) ) ;
#19371=EDGE_LOOP ( 'NONE', ( #14496, #16226, #7736, #14472, #19662 ) ) ;
#19384=VECTOR ( 'NONE', #7586, 1000.000000000000000 ) ;
#19418=ORIENTED_EDGE ( 'NONE', *, *, #16118, .F. ) ;
#19483=DIRECTION ( 'NONE',  ( 6.123031769111888756E-17, 0.000000000000000000, 1.000000000000000000 ) ) ;
#19657=PRODUCT_DEFINITION ( 'UNKNOWN', '', #10610, #10284 ) ;
#19662=ORIENTED_EDGE ( 'NONE', *, *, #12538, .F. ) ;
#19801=EDGE_CURVE ( 'NONE', #5105, #19851, #17119, .T. ) ;
#19828=LINE ( 'NONE', #7389, #10693 ) ;
#19851=VERTEX_POINT ( 'NONE', #727 ) ;
#20162=CLOSED_SHELL ( 'NONE', ( #4772, #5027, #20348, #15083, #6861, #3846, #13688 ) ) ;
#20261=CYLINDRICAL_SURFACE ( 'NONE', #1377, 3.000000000000000000 ) ;
#20348=ADVANCED_FACE ( 'NONE', ( #14202 ), #19022, .T. ) ;
ENDSEC;
END-ISO-10303-21;
